ISO-10303-21;
HEADER;
/* Generated by software containing ST-Developer
 * from STEP Tools, Inc. (www.steptools.com) 
 */

FILE_DESCRIPTION(
/* description */ ('Line shaft on three pillow blocks'),
/* implementation_level */ '2;1');

FILE_NAME(
/* name */ 'Mounting reducer bush (3).step',
/* time_stamp */ '2026-10-27T10:49:19-07:00',
/* author */ (''),
/* organization */ (''),
/* preprocessor_version */ 'ST-DEVELOPER v20.2',
/* originating_system */ 'Autodesk Translation Framework v15.17.0.0',
/* authorisation */ '');

FILE_SCHEMA (('AUTOMOTIVE_DESIGN { 1 0 10303 214 3 1 1 }'));
ENDSEC;

DATA;
#10=MECHANICAL_DESIGN_GEOMETRIC_PRESENTATION_REPRESENTATION('',(#346),#8377);
#292=SHAPE_REPRESENTATION_RELATIONSHIP('SRR','None',#8507,#319);
#319=ADVANCED_BREP_SHAPE_REPRESENTATION('',(#374),#8356);
#346=STYLED_ITEM('',(#8732),#374);
#374=MANIFOLD_SOLID_BREP('Body1',#4332);
#421=FACE_BOUND('',#999,.T.);
#422=FACE_BOUND('',#1001,.T.);
#528=PLANE('',#4770);
#529=PLANE('',#4771);
#714=FACE_OUTER_BOUND('',#996,.T.);
#715=FACE_OUTER_BOUND('',#997,.T.);
#716=FACE_OUTER_BOUND('',#998,.T.);
#717=FACE_OUTER_BOUND('',#1000,.T.);
#996=EDGE_LOOP('',(#3189,#3190,#3191,#3192));
#997=EDGE_LOOP('',(#3193,#3194,#3195,#3196));
#998=EDGE_LOOP('',(#3197));
#999=EDGE_LOOP('',(#3198));
#1000=EDGE_LOOP('',(#3199));
#1001=EDGE_LOOP('',(#3200));
#1335=LINE('',#6740,#1662);
#1336=LINE('',#6746,#1663);
#1662=VECTOR('',#5454,0.425);
#1663=VECTOR('',#5461,0.645);
#1949=CIRCLE('',#4765,0.425);
#1950=CIRCLE('',#4766,0.425);
#1951=CIRCLE('',#4768,0.645);
#1952=CIRCLE('',#4769,0.645);
#2148=VERTEX_POINT('',#6737);
#2149=VERTEX_POINT('',#6739);
#2150=VERTEX_POINT('',#6743);
#2151=VERTEX_POINT('',#6745);
#2543=EDGE_CURVE('',#2148,#2148,#1949,.T.);
#2544=EDGE_CURVE('',#2148,#2149,#1335,.T.);
#2545=EDGE_CURVE('',#2149,#2149,#1950,.T.);
#2546=EDGE_CURVE('',#2150,#2150,#1951,.T.);
#2547=EDGE_CURVE('',#2150,#2151,#1336,.T.);
#2548=EDGE_CURVE('',#2151,#2151,#1952,.T.);
#3189=ORIENTED_EDGE('',*,*,#2543,.F.);
#3190=ORIENTED_EDGE('',*,*,#2544,.T.);
#3191=ORIENTED_EDGE('',*,*,#2545,.T.);
#3192=ORIENTED_EDGE('',*,*,#2544,.F.);
#3193=ORIENTED_EDGE('',*,*,#2546,.F.);
#3194=ORIENTED_EDGE('',*,*,#2547,.T.);
#3195=ORIENTED_EDGE('',*,*,#2548,.T.);
#3196=ORIENTED_EDGE('',*,*,#2547,.F.);
#3197=ORIENTED_EDGE('',*,*,#2546,.T.);
#3198=ORIENTED_EDGE('',*,*,#2543,.T.);
#3199=ORIENTED_EDGE('',*,*,#2548,.F.);
#3200=ORIENTED_EDGE('',*,*,#2545,.F.);
#4021=CYLINDRICAL_SURFACE('',#4764,0.425);
#4022=CYLINDRICAL_SURFACE('',#4767,0.645);
#4132=ADVANCED_FACE('',(#714),#4021,.F.);
#4133=ADVANCED_FACE('',(#715),#4022,.T.);
#4134=ADVANCED_FACE('',(#716,#421),#528,.T.);
#4135=ADVANCED_FACE('',(#717,#422),#529,.F.);
#4332=CLOSED_SHELL('',(#4132,#4133,#4134,#4135));
#4763=AXIS2_PLACEMENT_3D('',#6735,#5448,#5449);
#4764=AXIS2_PLACEMENT_3D('',#6736,#5450,#5451);
#4765=AXIS2_PLACEMENT_3D('',#6738,#5452,#5453);
#4766=AXIS2_PLACEMENT_3D('',#6741,#5455,#5456);
#4767=AXIS2_PLACEMENT_3D('',#6742,#5457,#5458);
#4768=AXIS2_PLACEMENT_3D('',#6744,#5459,#5460);
#4769=AXIS2_PLACEMENT_3D('',#6747,#5462,#5463);
#4770=AXIS2_PLACEMENT_3D('',#6748,#5464,#5465);
#4771=AXIS2_PLACEMENT_3D('',#6749,#5466,#5467);
#5448=DIRECTION('axis',(0.,0.,1.));
#5449=DIRECTION('refdir',(1.,0.,0.));
#5450=DIRECTION('center_axis',(0.,0.,1.));
#5451=DIRECTION('ref_axis',(1.,0.,0.));
#5452=DIRECTION('center_axis',(0.,0.,-1.));
#5453=DIRECTION('ref_axis',(1.,0.,0.));
#5454=DIRECTION('',(0.,0.,-1.));
#5455=DIRECTION('center_axis',(0.,0.,-1.));
#5456=DIRECTION('ref_axis',(1.,0.,0.));
#5457=DIRECTION('center_axis',(0.,0.,1.));
#5458=DIRECTION('ref_axis',(1.,0.,0.));
#5459=DIRECTION('center_axis',(0.,0.,1.));
#5460=DIRECTION('ref_axis',(1.,0.,0.));
#5461=DIRECTION('',(0.,0.,-1.));
#5462=DIRECTION('center_axis',(0.,0.,1.));
#5463=DIRECTION('ref_axis',(1.,0.,0.));
#5464=DIRECTION('center_axis',(0.,0.,1.));
#5465=DIRECTION('ref_axis',(1.,0.,0.));
#5466=DIRECTION('center_axis',(0.,0.,1.));
#5467=DIRECTION('ref_axis',(1.,0.,0.));
#6735=CARTESIAN_POINT('',(0.,0.,0.));
#6736=CARTESIAN_POINT('Origin',(4.75,15.,1.2));
#6737=CARTESIAN_POINT('',(4.325,15.,2.4));
#6738=CARTESIAN_POINT('Origin',(4.75,15.,2.4));
#6739=CARTESIAN_POINT('',(4.325,15.,1.2));
#6740=CARTESIAN_POINT('',(4.325,15.,1.2));
#6741=CARTESIAN_POINT('Origin',(4.75,15.,1.2));
#6742=CARTESIAN_POINT('Origin',(4.75,15.,1.2));
#6743=CARTESIAN_POINT('',(4.105,15.,2.4));
#6744=CARTESIAN_POINT('Origin',(4.75,15.,2.4));
#6745=CARTESIAN_POINT('',(4.105,15.,1.2));
#6746=CARTESIAN_POINT('',(4.105,15.,1.2));
#6747=CARTESIAN_POINT('Origin',(4.75,15.,1.2));
#6748=CARTESIAN_POINT('Origin',(4.75,15.,2.4));
#6749=CARTESIAN_POINT('Origin',(4.75,15.,1.2));
#8324=UNCERTAINTY_MEASURE_WITH_UNIT(LENGTH_MEASURE(0.001),#8378,
'DISTANCE_ACCURACY_VALUE',
'Maximum model space distance between geometric entities at asserted c
onnectivities');
#8345=UNCERTAINTY_MEASURE_WITH_UNIT(LENGTH_MEASURE(0.001),#8378,
'DISTANCE_ACCURACY_VALUE',
'Maximum model space distance between geometric entities at asserted c
onnectivities');
#8356=(
GEOMETRIC_REPRESENTATION_CONTEXT(3)
GLOBAL_UNCERTAINTY_ASSIGNED_CONTEXT((#8324))
GLOBAL_UNIT_ASSIGNED_CONTEXT((#8378,#8380,#8381))
REPRESENTATION_CONTEXT('','3D')
);
#8377=(
GEOMETRIC_REPRESENTATION_CONTEXT(3)
GLOBAL_UNCERTAINTY_ASSIGNED_CONTEXT((#8345))
GLOBAL_UNIT_ASSIGNED_CONTEXT((#8378,#8380,#8381))
REPRESENTATION_CONTEXT('','3D')
);
#8378=(
LENGTH_UNIT()
NAMED_UNIT(*)
SI_UNIT(.CENTI.,.METRE.)
);
#8380=(
NAMED_UNIT(*)
PLANE_ANGLE_UNIT()
SI_UNIT($,.RADIAN.)
);
#8381=(
NAMED_UNIT(*)
SI_UNIT($,.STERADIAN.)
SOLID_ANGLE_UNIT()
);
#8392=SHAPE_DEFINITION_REPRESENTATION(#8423,#8507);
#8423=PRODUCT_DEFINITION_SHAPE('',$,#8539);
#8507=SHAPE_REPRESENTATION('',(#4763),#8356);
#8528=PRODUCT_DEFINITION_CONTEXT('part definition',#8623,'design');
#8539=PRODUCT_DEFINITION('Mounting reducer bush (3)',
'Mounting reducer bush (3)',#8570,#8528);
#8570=PRODUCT_DEFINITION_FORMATION('',$,#8635);
#8623=APPLICATION_CONTEXT(
'Core Data for Automotive Mechanical Design Process');
#8624=PRODUCT_CONTEXT('part definition',#8623,'mechanical');
#8635=PRODUCT('Mounting reducer bush (3)','Mounting reducer bush (3)',
'Mounting reducer bush (3)',(#8624));
#8726=COLOUR_RGB('Off White',0.89,0.88,0.83);
#8727=FILL_AREA_STYLE_COLOUR('',#8726);
#8728=FILL_AREA_STYLE('',(#8727));
#8729=SURFACE_STYLE_FILL_AREA(#8728);
#8730=SURFACE_SIDE_STYLE('',(#8729));
#8731=SURFACE_STYLE_USAGE(.BOTH.,#8730);
#8732=PRESENTATION_STYLE_ASSIGNMENT((#8731));
ENDSEC;
END-ISO-10303-21;
